ISO-10303-21;
HEADER;
/* Generated by software containing ST-Developer
 * from STEP Tools, Inc. (www.steptools.com) 
 */

FILE_DESCRIPTION(
/* description */ (''),
/* implementation_level */ '2;1');

FILE_NAME(
/* name */ '11_Dial_Axle_Pin_3x39.step',
/* time_stamp */ '2026-10-25T01:30:15-07:00',
/* author */ (''),
/* organization */ (''),
/* preprocessor_version */ 'ST-DEVELOPER v20.2',
/* originating_system */ 'Autodesk Translation Framework v15.15.0.0',
/* authorisation */ '');

FILE_SCHEMA (('AUTOMOTIVE_DESIGN { 1 0 10303 214 3 1 1 }'));
ENDSEC;

DATA;
#10=MECHANICAL_DESIGN_GEOMETRIC_PRESENTATION_REPRESENTATION('',(#572),#32309);
#544=SHAPE_REPRESENTATION_RELATIONSHIP('SRR','None',#32371,#558);
#558=ADVANCED_BREP_SHAPE_REPRESENTATION('',(#586),#32304);
#572=STYLED_ITEM('',(#32502),#586);
#586=MANIFOLD_SOLID_BREP('Body1',#13813);
#743=CYLINDRICAL_SURFACE('',#14632,1.5);
#1017=CIRCLE('',#14629,1.2);
#1018=CIRCLE('',#14631,1.5);
#1019=CIRCLE('',#14633,1.5);
#1020=CIRCLE('',#14635,1.2);
#1206=CONICAL_SURFACE('',#14630,1.35,0.785398163397448);
#1207=CONICAL_SURFACE('',#14634,1.35,0.785398163397451);
#1718=FACE_OUTER_BOUND('',#2568,.T.);
#1719=FACE_OUTER_BOUND('',#2569,.T.);
#1720=FACE_OUTER_BOUND('',#2570,.T.);
#1721=FACE_OUTER_BOUND('',#2571,.T.);
#1722=FACE_OUTER_BOUND('',#2572,.T.);
#2568=EDGE_LOOP('',(#10937));
#2569=EDGE_LOOP('',(#10938,#10939,#10940,#10941));
#2570=EDGE_LOOP('',(#10942,#10943,#10944,#10945));
#2571=EDGE_LOOP('',(#10946,#10947,#10948,#10949));
#2572=EDGE_LOOP('',(#10950));
#3565=LINE('',#26531,#4876);
#3566=LINE('',#26535,#4877);
#3567=LINE('',#26539,#4878);
#4876=VECTOR('',#16991,1.35);
#4877=VECTOR('',#16996,1.5);
#4878=VECTOR('',#17001,1.35);
#6194=VERTEX_POINT('',#26526);
#6195=VERTEX_POINT('',#26529);
#6196=VERTEX_POINT('',#26533);
#6197=VERTEX_POINT('',#26537);
#7845=EDGE_CURVE('',#6194,#6194,#1017,.T.);
#7846=EDGE_CURVE('',#6195,#6195,#1018,.T.);
#7847=EDGE_CURVE('',#6195,#6194,#3565,.T.);
#7848=EDGE_CURVE('',#6196,#6196,#1019,.T.);
#7849=EDGE_CURVE('',#6196,#6195,#3566,.T.);
#7850=EDGE_CURVE('',#6197,#6197,#1020,.T.);
#7851=EDGE_CURVE('',#6197,#6196,#3567,.T.);
#10937=ORIENTED_EDGE('',*,*,#7845,.F.);
#10938=ORIENTED_EDGE('',*,*,#7846,.F.);
#10939=ORIENTED_EDGE('',*,*,#7847,.T.);
#10940=ORIENTED_EDGE('',*,*,#7845,.T.);
#10941=ORIENTED_EDGE('',*,*,#7847,.F.);
#10942=ORIENTED_EDGE('',*,*,#7848,.F.);
#10943=ORIENTED_EDGE('',*,*,#7849,.T.);
#10944=ORIENTED_EDGE('',*,*,#7846,.T.);
#10945=ORIENTED_EDGE('',*,*,#7849,.F.);
#10946=ORIENTED_EDGE('',*,*,#7850,.F.);
#10947=ORIENTED_EDGE('',*,*,#7851,.T.);
#10948=ORIENTED_EDGE('',*,*,#7848,.T.);
#10949=ORIENTED_EDGE('',*,*,#7851,.F.);
#10950=ORIENTED_EDGE('',*,*,#7850,.T.);
#12796=PLANE('',#14628);
#12797=PLANE('',#14636);
#13481=ADVANCED_FACE('',(#1718),#12796,.T.);
#13482=ADVANCED_FACE('',(#1719),#1206,.T.);
#13483=ADVANCED_FACE('',(#1720),#743,.T.);
#13484=ADVANCED_FACE('',(#1721),#1207,.T.);
#13485=ADVANCED_FACE('',(#1722),#12797,.T.);
#13813=CLOSED_SHELL('',(#13481,#13482,#13483,#13484,#13485));
#14627=AXIS2_PLACEMENT_3D('',#26524,#16981,#16982);
#14628=AXIS2_PLACEMENT_3D('',#26525,#16983,#16984);
#14629=AXIS2_PLACEMENT_3D('',#26527,#16985,#16986);
#14630=AXIS2_PLACEMENT_3D('',#26528,#16987,#16988);
#14631=AXIS2_PLACEMENT_3D('',#26530,#16989,#16990);
#14632=AXIS2_PLACEMENT_3D('',#26532,#16992,#16993);
#14633=AXIS2_PLACEMENT_3D('',#26534,#16994,#16995);
#14634=AXIS2_PLACEMENT_3D('',#26536,#16997,#16998);
#14635=AXIS2_PLACEMENT_3D('',#26538,#16999,#17000);
#14636=AXIS2_PLACEMENT_3D('',#26540,#17002,#17003);
#16981=DIRECTION('axis',(0.,0.,1.));
#16982=DIRECTION('refdir',(1.,0.,0.));
#16983=DIRECTION('center_axis',(-1.,0.,0.));
#16984=DIRECTION('ref_axis',(0.,0.,1.));
#16985=DIRECTION('center_axis',(1.,0.,0.));
#16986=DIRECTION('ref_axis',(0.,0.,-1.));
#16987=DIRECTION('center_axis',(1.,0.,0.));
#16988=DIRECTION('ref_axis',(0.,1.,0.));
#16989=DIRECTION('center_axis',(1.,0.,0.));
#16990=DIRECTION('ref_axis',(0.,0.,-1.));
#16991=DIRECTION('',(-0.707106781186547,0.707106781186548,8.65956056235493E-17));
#16992=DIRECTION('center_axis',(1.,0.,0.));
#16993=DIRECTION('ref_axis',(0.,1.,0.));
#16994=DIRECTION('center_axis',(1.,0.,0.));
#16995=DIRECTION('ref_axis',(0.,0.,-1.));
#16996=DIRECTION('',(-1.,0.,0.));
#16997=DIRECTION('center_axis',(-1.,0.,0.));
#16998=DIRECTION('ref_axis',(0.,1.,0.));
#16999=DIRECTION('center_axis',(1.,0.,0.));
#17000=DIRECTION('ref_axis',(0.,0.,-1.));
#17001=DIRECTION('',(-0.707106781186545,-0.70710678118655,-8.65956056235496E-17));
#17002=DIRECTION('center_axis',(1.,0.,0.));
#17003=DIRECTION('ref_axis',(0.,0.,-1.));
#26524=CARTESIAN_POINT('',(0.,0.,0.));
#26525=CARTESIAN_POINT('Origin',(0.,1.2,0.));
#26526=CARTESIAN_POINT('',(5.3776427755281E-16,-1.2,-1.46957615897682E-16));
#26527=CARTESIAN_POINT('Origin',(0.,0.,0.));
#26528=CARTESIAN_POINT('Origin',(0.150000000000001,0.,0.));
#26529=CARTESIAN_POINT('',(0.3,-1.5,-1.83697019872103E-16));
#26530=CARTESIAN_POINT('Origin',(0.299999999999998,0.,0.));
#26531=CARTESIAN_POINT('',(0.150000000000001,-1.35,-1.65327317884893E-16));
#26532=CARTESIAN_POINT('Origin',(19.5,0.,0.));
#26533=CARTESIAN_POINT('',(38.7,-1.5,-1.83697019872103E-16));
#26534=CARTESIAN_POINT('Origin',(38.7,0.,0.));
#26535=CARTESIAN_POINT('',(19.5,-1.5,-1.83697019872103E-16));
#26536=CARTESIAN_POINT('Origin',(38.85,0.,0.));
#26537=CARTESIAN_POINT('',(39.,-1.2,-1.46957615897682E-16));
#26538=CARTESIAN_POINT('Origin',(39.,0.,0.));
#26539=CARTESIAN_POINT('',(38.85,-1.35,-1.65327317884893E-16));
#26540=CARTESIAN_POINT('Origin',(39.,0.,0.));
#32288=UNCERTAINTY_MEASURE_WITH_UNIT(LENGTH_MEASURE(0.01),#32310,
'DISTANCE_ACCURACY_VALUE',
'Maximum model space distance between geometric entities at asserted c
onnectivities');
#32293=UNCERTAINTY_MEASURE_WITH_UNIT(LENGTH_MEASURE(0.01),#32310,
'DISTANCE_ACCURACY_VALUE',
'Maximum model space distance between geometric entities at asserted c
onnectivities');
#32304=(
GEOMETRIC_REPRESENTATION_CONTEXT(3)
GLOBAL_UNCERTAINTY_ASSIGNED_CONTEXT((#32288))
GLOBAL_UNIT_ASSIGNED_CONTEXT((#32310,#32312,#32313))
REPRESENTATION_CONTEXT('','3D')
);
#32309=(
GEOMETRIC_REPRESENTATION_CONTEXT(3)
GLOBAL_UNCERTAINTY_ASSIGNED_CONTEXT((#32293))
GLOBAL_UNIT_ASSIGNED_CONTEXT((#32310,#32312,#32313))
REPRESENTATION_CONTEXT('','3D')
);
#32310=(
LENGTH_UNIT()
NAMED_UNIT(*)
SI_UNIT(.MILLI.,.METRE.)
);
#32312=(
NAMED_UNIT(*)
PLANE_ANGLE_UNIT()
SI_UNIT($,.RADIAN.)
);
#32313=(
NAMED_UNIT(*)
SI_UNIT($,.STERADIAN.)
SOLID_ANGLE_UNIT()
);
#32324=SHAPE_DEFINITION_REPRESENTATION(#32339,#32371);
#32339=PRODUCT_DEFINITION_SHAPE('',$,#32387);
#32371=SHAPE_REPRESENTATION('',(#14627),#32304);
#32376=PRODUCT_DEFINITION_CONTEXT('part definition',#32423,'design');
#32387=PRODUCT_DEFINITION('2026-10-25-00-35-20-536',
'11_Dial_Axle_Pin_3x39',#32402,#32376);
#32402=PRODUCT_DEFINITION_FORMATION('',$,#32435);
#32423=APPLICATION_CONTEXT(
'Core Data for Automotive Mechanical Design Process');
#32424=PRODUCT_CONTEXT('part definition',#32423,'mechanical');
#32435=PRODUCT('2026-10-25-00-35-20-536','11_Dial_Axle_Pin_3x39',$,(#32424));
#32496=COLOUR_RGB('Grey',0.48,0.52,0.57);
#32497=FILL_AREA_STYLE_COLOUR('',#32496);
#32498=FILL_AREA_STYLE('',(#32497));
#32499=SURFACE_STYLE_FILL_AREA(#32498);
#32500=SURFACE_SIDE_STYLE('',(#32499));
#32501=SURFACE_STYLE_USAGE(.BOTH.,#32500);
#32502=PRESENTATION_STYLE_ASSIGNMENT((#32501));
ENDSEC;
END-ISO-10303-21;
